ISO-10303-21;
HEADER;
FILE_DESCRIPTION (('STEP AP214'),
    '1' );
FILE_NAME ('Latch Lock Pin Wire.step',
    '2026-10-09T19:32:29',
    ( '' ),
    ( '' ),
    'SwSTEP 2.0',
    'SolidWorks 2026',
    '' );
FILE_SCHEMA (( 'AUTOMOTIVE_DESIGN' ));
ENDSEC;

DATA;
#4=SURFACE_STYLE_USAGE ( .BOTH. , #13787 ) ;
#18=CYLINDRICAL_SURFACE ( 'NONE', #7513, 0.2500000000000002220 ) ;
#96=DIRECTION ( 'NONE',  ( 6.123233995736769734E-17, 0.000000000000000000, 1.000000000000000000 ) ) ;
#156=ORIENTED_EDGE ( 'NONE', *, *, #7147, .T. ) ;
#207=EDGE_CURVE ( 'NONE', #14363, #4874, #14274, .T. ) ;
#209=CARTESIAN_POINT ( 'NONE',  ( 1.836970198721030057E-17, 2.299999999999999822, 7.700000000000000178 ) ) ;
#281=DIRECTION ( 'NONE',  ( 0.000000000000000000, 1.000000000000000000, 0.000000000000000000 ) ) ;
#284=CARTESIAN_POINT ( 'NONE',  ( -6.735557395310430190E-17, 7.000000000000000000, 6.299999999999999822 ) ) ;
#341=FACE_OUTER_BOUND ( 'NONE', #1960, .T. ) ;
#343=CARTESIAN_POINT ( 'NONE',  ( -6.735557395310420329E-17, 6.700000000000000178, 6.299999999999999822 ) ) ;
#395=FACE_OUTER_BOUND ( 'NONE', #17771, .T. ) ;
#417=EDGE_CURVE ( 'NONE', #7791, #16660, #1347, .T. ) ;
#463=ADVANCED_FACE ( 'NONE', ( #6664 ), #1664, .T. ) ;
#468=DIRECTION ( 'NONE',  ( 6.123233995736769734E-17, 9.462128050782581713E-15, 1.000000000000000000 ) ) ;
#501=AXIS2_PLACEMENT_3D ( 'NONE', #17888, #13465, #603 ) ;
#506=DIRECTION ( 'NONE',  ( 1.000000000000000000, 1.283953296258166085E-32, -6.123233995736769734E-17 ) ) ;
#510=EDGE_CURVE ( 'NONE', #2436, #16660, #16741, .T. ) ;
#513=CIRCLE ( 'NONE', #1410, 0.2500000000000002220 ) ;
#517=EDGE_LOOP ( 'NONE', ( #11060, #3583, #4007, #16442 ) ) ;
#529=AXIS2_PLACEMENT_3D ( 'NONE', #9899, #3969, #6850 ) ;
#549=ORIENTED_EDGE ( 'NONE', *, *, #17371, .T. ) ;
#601=CARTESIAN_POINT ( 'NONE',  ( 5.829811056852189859E-17, 3.957026083511942627, 8.102080397533576672 ) ) ;
#603=DIRECTION ( 'NONE',  ( 1.836970198721028208E-16, -6.938893903907222067E-15, 1.000000000000000000 ) ) ;
#612=CARTESIAN_POINT ( 'NONE',  ( -3.992840858131154872E-17, 4.942973916488066166, 6.497919602466422084 ) ) ;
#689=ADVANCED_FACE ( 'NONE', ( #2688 ), #9940, .T. ) ;
#725=DIRECTION ( 'NONE',  ( -1.000000000000000000, 0.000000000000000000, 1.224646799147350002E-16 ) ) ;
#799=ORIENTED_EDGE ( 'NONE', *, *, #16349, .F. ) ;
#814=DIRECTION ( 'NONE',  ( 6.123233995736806712E-17, 0.000000000000000000, 1.000000000000000000 ) ) ;
#832=EDGE_LOOP ( 'NONE', ( #16640, #4367, #7529, #3942 ) ) ;
#895=CIRCLE ( 'NONE', #17419, 0.5500000000000001554 ) ;
#1076=DIRECTION ( 'NONE',  ( 6.123233995736764803E-17, 1.000000000000000000, 0.000000000000000000 ) ) ;
#1078=ORIENTED_EDGE ( 'NONE', *, *, #10764, .F. ) ;
#1085=CLOSED_SHELL ( 'NONE', ( #9768, #689, #15955, #463, #18050, #1932, #10094, #5396, #1581, #3025, #2151, #11551, #5849, #5340, #16454, #1491, #3707, #14394, #14927, #5854 ) ) ;
#1089=CARTESIAN_POINT ( 'NONE',  ( 3.179896940101190659E-17, 3.786446520921929793, 7.919316580472860245 ) ) ;
#1106=VERTEX_POINT ( 'NONE', #8300 ) ;
#1115=CARTESIAN_POINT ( 'NONE',  ( 3.673940397442067510E-17, 3.581751045813930112, 7.750000000000000000 ) ) ;
#1249=DIRECTION ( 'NONE',  ( 3.018987445473099952E-48, 1.000000000000000000, 2.465190328815659976E-32 ) ) ;
#1347=CIRCLE ( 'NONE', #10824, 0.5500000000000001554 ) ;
#1359=EDGE_LOOP ( 'NONE', ( #549, #15650, #7823, #5403 ) ) ;
#1410=AXIS2_PLACEMENT_3D ( 'NONE', #9640, #2616, #2796 ) ;
#1491=ADVANCED_FACE ( 'NONE', ( #5722 ), #12670, .T. ) ;
#1499=AXIS2_PLACEMENT_3D ( 'NONE', #6840, #4048, #11369 ) ;
#1521=ORIENTED_EDGE ( 'NONE', *, *, #4349, .F. ) ;
#1550=DIRECTION ( 'NONE',  ( -6.161988852941170860E-64, -1.000000000000000000, 3.773129962568039733E-80 ) ) ;
#1581=ADVANCED_FACE ( 'NONE', ( #7289 ), #12935, .T. ) ;
#1610=ORIENTED_EDGE ( 'NONE', *, *, #10246, .F. ) ;
#1633=DIRECTION ( 'NONE',  ( 0.000000000000000000, 0.000000000000000000, 1.000000000000000000 ) ) ;
#1638=DIRECTION ( 'NONE',  ( -4.476422471267237545E-17, -0.6823182503600040416, -0.7310552682428754778 ) ) ;
#1658=CARTESIAN_POINT ( 'NONE',  ( -4.898587196589400133E-17, 5.318248954186070243, 6.599999999999999645 ) ) ;
#1664=TOROIDAL_SURFACE ( 'NONE', #9645, 0.2999999999999999889, 0.2500000000000000000 ) ;
#1666=CARTESIAN_POINT ( 'NONE',  ( 3.673940397442059498E-17, 2.600000000000000089, 8.000000000000000000 ) ) ;
#1681=CARTESIAN_POINT ( 'NONE',  ( 4.898587196589403214E-17, 2.600000000000000089, 7.700000000000000178 ) ) ;
#1785=VERTEX_POINT ( 'NONE', #612 ) ;
#1829=DIRECTION ( 'NONE',  ( 6.123233995736764803E-17, 1.000000000000000000, 0.000000000000000000 ) ) ;
#1840=EDGE_CURVE ( 'NONE', #10043, #4420, #5695, .T. ) ;
#1856=CARTESIAN_POINT ( 'NONE',  ( -3.061616997868258372E-18, 5.318248954186068467, 6.850000000000000533 ) ) ;
#1861=DIRECTION ( 'NONE',  ( 3.018987445473109675E-48, 1.000000000000000000, 2.465190328815659976E-32 ) ) ;
#1898=DIRECTION ( 'NONE',  ( -4.177994306516050823E-17, 0.7310552682428690385, -0.6823182503600111470 ) ) ;
#1929=CARTESIAN_POINT ( 'NONE',  ( 1.836970198721020197E-17, 3.581751045813930112, 7.700000000000000178 ) ) ;
#1932=ADVANCED_FACE ( 'NONE', ( #16941 ), #18, .T. ) ;
#1943=VERTEX_POINT ( 'NONE', #4251 ) ;
#1960=EDGE_LOOP ( 'NONE', ( #11728, #16378, #7363, #4476 ) ) ;
#1962=AXIS2_PLACEMENT_3D ( 'NONE', #5821, #15388, #2971 ) ;
#1980=ORIENTED_EDGE ( 'NONE', *, *, #7793, .T. ) ;
#2036=CARTESIAN_POINT ( 'NONE',  ( -1.408343819019460219E-16, 2.299999999999999822, 5.100000000000000533 ) ) ;
#2047=PRODUCT_CONTEXT ( 'NONE', #16913, 'mechanical' ) ;
#2117=ORIENTED_EDGE ( 'NONE', *, *, #7793, .F. ) ;
#2151=ADVANCED_FACE ( 'NONE', ( #9145 ), #14806, .T. ) ;
#2157=DIRECTION ( 'NONE',  ( 1.224646799147349016E-16, 0.000000000000000000, 1.000000000000000000 ) ) ;
#2171=ORIENTED_EDGE ( 'NONE', *, *, #7588, .T. ) ;
#2202=DIRECTION ( 'NONE',  ( -4.476422471267237545E-17, -0.6823182503600040416, -0.7310552682428754778 ) ) ;
#2215=FACE_OUTER_BOUND ( 'NONE', #14632, .T. ) ;
#2218=EDGE_LOOP ( 'NONE', ( #16432, #2171, #13323, #1521 ) ) ;
#2336=AXIS2_PLACEMENT_3D ( 'NONE', #13345, #3420, #15961 ) ;
#2355=AXIS2_PLACEMENT_3D ( 'NONE', #12983, #1861, #6115 ) ;
#2385=AXIS2_PLACEMENT_3D ( 'NONE', #14120, #14223, #8573 ) ;
#2436=VERTEX_POINT ( 'NONE', #5192 ) ;
#2515=VERTEX_POINT ( 'NONE', #7959 ) ;
#2556=DIRECTION ( 'NONE',  ( 6.123233995736767268E-17, 1.000000000000000000, 0.000000000000000000 ) ) ;
#2591=( LENGTH_UNIT ( ) NAMED_UNIT ( * ) SI_UNIT ( .MILLI., .METRE. ) );
#2608=AXIS2_PLACEMENT_3D ( 'NONE', #6376, #9161, #468 ) ;
#2616=DIRECTION ( 'NONE',  ( -6.123233995736769734E-17, -8.820551857043939970E-15, -1.000000000000000000 ) ) ;
#2643=CARTESIAN_POINT ( 'NONE',  ( -1.255262969126040791E-16, 7.250000000000000000, 5.100000000000000533 ) ) ;
#2688=FACE_OUTER_BOUND ( 'NONE', #3433, .T. ) ;
#2690=LINE ( 'NONE', #9727, #9050 ) ;
#2734=DIRECTION ( 'NONE',  ( -1.000000000000000000, 6.161988852941170860E-64, 6.123233995736769734E-17 ) ) ;
#2774=AXIS2_PLACEMENT_3D ( 'NONE', #7737, #6071, #1829 ) ;
#2796=DIRECTION ( 'NONE',  ( -6.740754805355319355E-31, 1.000000000000000000, -1.040834085586083310E-14 ) ) ;
#2863=FILL_AREA_STYLE ('',( #2966 ) ) ;
#2966=FILL_AREA_STYLE_COLOUR ( '', #5562 ) ;
#2969=LINE ( 'NONE', #601, #9009 ) ;
#2971=DIRECTION ( 'NONE',  ( 1.224646799147349016E-16, 0.000000000000000000, 1.000000000000000000 ) ) ;
#2987=DIRECTION ( 'NONE',  ( -1.000000000000000000, 0.000000000000000000, 6.123233995736769734E-17 ) ) ;
#3006=ORIENTED_EDGE ( 'NONE', *, *, #4825, .T. ) ;
#3025=ADVANCED_FACE ( 'NONE', ( #12246 ), #17868, .F. ) ;
#3142=CARTESIAN_POINT ( 'NONE',  ( -3.061616997868380553E-17, 5.318248954186070243, 6.899999999999999467 ) ) ;
#3145=CARTESIAN_POINT ( 'NONE',  ( -1.408343819019460219E-16, 7.000000000000000000, 5.100000000000000533 ) ) ;
#3200=DIRECTION ( 'NONE',  ( -1.000000000000000000, 6.161988852941170860E-64, 6.123233995736769734E-17 ) ) ;
#3219=CIRCLE ( 'NONE', #12088, 0.04999999999999969746 ) ;
#3275=CARTESIAN_POINT ( 'NONE',  ( -4.898587196589400133E-17, 5.318248954186070243, 6.599999999999999645 ) ) ;
#3293=FACE_OUTER_BOUND ( 'NONE', #9550, .T. ) ;
#3334=DIRECTION ( 'NONE',  ( 6.123233995736769734E-17, 8.894960955186829541E-48, 1.000000000000000000 ) ) ;
#3356=EDGE_LOOP ( 'NONE', ( #5368, #10630, #16215, #17214 ) ) ;
#3370=ORIENTED_EDGE ( 'NONE', *, *, #11676, .T. ) ;
#3411=AXIS2_PLACEMENT_3D ( 'NONE', #11384, #7047, #96 ) ;
#3420=DIRECTION ( 'NONE',  ( 6.123233995736769734E-17, 8.894960955186829541E-48, 1.000000000000000000 ) ) ;
#3433=EDGE_LOOP ( 'NONE', ( #4165, #8700, #11689, #7623 ) ) ;
#3569=ORIENTED_EDGE ( 'NONE', *, *, #16349, .T. ) ;
#3583=ORIENTED_EDGE ( 'NONE', *, *, #6705, .T. ) ;
#3652=DIRECTION ( 'NONE',  ( 5.296209390990920866E-31, 1.000000000000000000, 8.548717289613711672E-15 ) ) ;
#3653=DIRECTION ( 'NONE',  ( -4.177994306516039113E-17, 0.7310552682428709259, -0.6823182503600090376 ) ) ;
#3670=CARTESIAN_POINT ( 'NONE',  ( -3.061616997868380553E-17, 5.318248954186070243, 6.899999999999999467 ) ) ;
#3674=AXIS2_PLACEMENT_3D ( 'NONE', #7767, #13412, #725 ) ;
#3693=AXIS2_PLACEMENT_3D ( 'NONE', #10327, #1898, #17705 ) ;
#3698=EDGE_LOOP ( 'NONE', ( #16861, #3569, #17508, #9473 ) ) ;
#3707=ADVANCED_FACE ( 'NONE', ( #2215 ), #15600, .T. ) ;
#3757=CIRCLE ( 'NONE', #501, 0.2500000000000002220 ) ;
#3820=DIRECTION ( 'NONE',  ( 1.000000000000000000, 0.000000000000000000, 0.000000000000000000 ) ) ;
#3848=CARTESIAN_POINT ( 'NONE',  ( 3.179896940101190659E-17, 3.786446520921940007, 7.919316580472860245 ) ) ;
#3893=ORIENTED_EDGE ( 'NONE', *, *, #11288, .F. ) ;
#3942=ORIENTED_EDGE ( 'NONE', *, *, #4825, .F. ) ;
#3969=DIRECTION ( 'NONE',  ( -4.177994306516050823E-17, 0.7310552682428690385, -0.6823182503600111470 ) ) ;
#3986=CARTESIAN_POINT ( 'NONE',  ( -1.255262969126041037E-16, 2.550000000000000266, 5.100000000000000533 ) ) ;
#3999=DIRECTION ( 'NONE',  ( 1.836970198721028208E-16, -6.938893903907222067E-15, 1.000000000000000000 ) ) ;
#4007=ORIENTED_EDGE ( 'NONE', *, *, #4183, .T. ) ;
#4048=DIRECTION ( 'NONE',  ( 1.000000000000000000, 1.283953296258166085E-32, -6.123233995736769734E-17 ) ) ;
#4062=AXIS2_PLACEMENT_3D ( 'NONE', #11448, #506, #1638 ) ;
#4115=CARTESIAN_POINT ( 'NONE',  ( 5.204748896376257478E-17, 2.600000000000000089, 8.250000000000000000 ) ) ;
#4119=PRODUCT_DEFINITION_FORMATION_WITH_SPECIFIED_SOURCE ( 'ANY', '', #6678, .NOT_KNOWN. ) ;
#4143=EDGE_LOOP ( 'NONE', ( #17872, #1980, #5813, #3893 ) ) ;
#4146=DIRECTION ( 'NONE',  ( 1.000000000000000000, 0.000000000000000000, 0.000000000000000000 ) ) ;
#4165=ORIENTED_EDGE ( 'NONE', *, *, #8662, .T. ) ;
#4167=ORIENTED_EDGE ( 'NONE', *, *, #11288, .T. ) ;
#4183=EDGE_CURVE ( 'NONE', #12988, #7791, #12710, .T. ) ;
#4249=APPLICATION_CONTEXT ( 'automotive_design' ) ;
#4251=CARTESIAN_POINT ( 'NONE',  ( -1.836970198721025435E-17, 6.700000000000000178, 6.850000000000000533 ) ) ;
#4269=DIRECTION ( 'NONE',  ( -6.123233995736769734E-17, 3.749399456654650178E-33, -1.000000000000000000 ) ) ;
#4335=CYLINDRICAL_SURFACE ( 'NONE', #9993, 0.2500000000000002220 ) ;
#4349=EDGE_CURVE ( 'NONE', #4874, #15355, #12377, .T. ) ;
#4367=ORIENTED_EDGE ( 'NONE', *, *, #7004, .T. ) ;
#4382=PRODUCT_DEFINITION ( 'UNKNOWN', '', #4119, #5473 ) ;
#4420=VERTEX_POINT ( 'NONE', #1856 ) ;
#4476=ORIENTED_EDGE ( 'NONE', *, *, #11676, .F. ) ;
#4658=ADVANCED_BREP_SHAPE_REPRESENTATION ( '', ( #7985, #17681 ), #12699 ) ;
#4796=DIRECTION ( 'NONE',  ( -6.123233995736767268E-17, 0.000000000000000000, -1.000000000000000000 ) ) ;
#4805=EDGE_CURVE ( 'NONE', #1785, #17654, #7254, .T. ) ;
#4825=EDGE_CURVE ( 'NONE', #5242, #17654, #2969, .T. ) ;
#4874=VERTEX_POINT ( 'NONE', #6322 ) ;
#4916=EDGE_LOOP ( 'NONE', ( #8813, #17383, #3006, #13142 ) ) ;
#4936=CIRCLE ( 'NONE', #15320, 0.5500000000000001554 ) ;
#4998=AXIS2_PLACEMENT_3D ( 'NONE', #11731, #17365, #10343 ) ;
#5004=FACE_OUTER_BOUND ( 'NONE', #517, .T. ) ;
#5143=FACE_OUTER_BOUND ( 'NONE', #2218, .T. ) ;
#5192=CARTESIAN_POINT ( 'NONE',  ( 3.673940397442067510E-17, 2.600000000000000089, 7.750000000000000000 ) ) ;
#5206=DIRECTION ( 'NONE',  ( 0.000000000000000000, 0.000000000000000000, 1.000000000000000000 ) ) ;
#5242=VERTEX_POINT ( 'NONE', #12630 ) ;
#5325=ORIENTED_EDGE ( 'NONE', *, *, #8622, .F. ) ;
#5340=ADVANCED_FACE ( 'NONE', ( #17503 ), #8915, .T. ) ;
#5368=ORIENTED_EDGE ( 'NONE', *, *, #16510, .T. ) ;
#5396=ADVANCED_FACE ( 'NONE', ( #8781 ), #4335, .T. ) ;
#5403=ORIENTED_EDGE ( 'NONE', *, *, #9175, .F. ) ;
#5473=PRODUCT_DEFINITION_CONTEXT ( 'detailed design', #4249, 'design' ) ;
#5479=DIRECTION ( 'NONE',  ( 6.123233995736806712E-17, 0.000000000000000000, 1.000000000000000000 ) ) ;
#5533=CIRCLE ( 'NONE', #15883, 0.2500000000000002220 ) ;
#5546=( LENGTH_UNIT ( ) NAMED_UNIT ( * ) SI_UNIT ( .MILLI., .METRE. ) );
#5562=COLOUR_RGB ( '', 0.08235294, 0.09019608, 0.10196078) ;
#5624=DIRECTION ( 'NONE',  ( 6.123233995736767268E-17, -1.000000000000000000, 0.000000000000000000 ) ) ;
#5645=EDGE_CURVE ( 'NONE', #18075, #15355, #10284, .T. ) ;
#5690=ORIENTED_EDGE ( 'NONE', *, *, #5645, .F. ) ;
#5695=CIRCLE ( 'NONE', #7180, 0.2500000000000002220 ) ;
#5717=AXIS2_PLACEMENT_3D ( 'NONE', #17090, #17001, #15728 ) ;
#5722=FACE_OUTER_BOUND ( 'NONE', #4916, .T. ) ;
#5785=ORIENTED_EDGE ( 'NONE', *, *, #10780, .T. ) ;
#5801=VERTEX_POINT ( 'NONE', #10453 ) ;
#5813=ORIENTED_EDGE ( 'NONE', *, *, #16510, .F. ) ;
#5821=CARTESIAN_POINT ( 'NONE',  ( -4.898587196589400133E-17, 6.700000000000000178, 6.599999999999999645 ) ) ;
#5841=CARTESIAN_POINT ( 'NONE',  ( 4.898587196589403214E-17, 3.581751045813930112, 7.700000000000000178 ) ) ;
#5849=ADVANCED_FACE ( 'NONE', ( #9258 ), #8809, .T. ) ;
#5854=ADVANCED_FACE ( 'NONE', ( #5004 ), #6287, .T. ) ;
#5915=CIRCLE ( 'NONE', #14770, 0.2500000000000002220 ) ;
#5923=DIRECTION ( 'NONE',  ( -6.123233995736769734E-17, -8.820551857043939970E-15, -1.000000000000000000 ) ) ;
#5936=DIRECTION ( 'NONE',  ( -1.000000000000000000, 6.161988852941170860E-64, 6.123233995736769734E-17 ) ) ;
#5994=DIRECTION ( 'NONE',  ( 0.000000000000000000, 0.000000000000000000, 1.000000000000000000 ) ) ;
#6017=CARTESIAN_POINT ( 'NONE',  ( 1.836970198721020197E-17, 2.600000000000000089, 7.700000000000000178 ) ) ;
#6071=DIRECTION ( 'NONE',  ( -6.123233995736769734E-17, 3.749399456654650178E-33, -1.000000000000000000 ) ) ;
#6097=DIRECTION ( 'NONE',  ( 6.123233995736769734E-17, 0.000000000000000000, 1.000000000000000000 ) ) ;
#6106=CIRCLE ( 'NONE', #1962, 0.2500000000000002220 ) ;
#6108=EDGE_CURVE ( 'NONE', #4420, #1943, #2690, .T. ) ;
#6115=DIRECTION ( 'NONE',  ( 1.224646799147349263E-16, 0.000000000000000000, 1.000000000000000000 ) ) ;
#6126=SHAPE_DEFINITION_REPRESENTATION ( #6985, #16473 ) ;
#6138=AXIS2_PLACEMENT_3D ( 'NONE', #15526, #12639, #18264 ) ;
#6224=ORIENTED_EDGE ( 'NONE', *, *, #4183, .F. ) ;
#6240=DIRECTION ( 'NONE',  ( -4.177994306516050823E-17, 0.7310552682428690385, -0.6823182503600111470 ) ) ;
#6273=ORIENTED_EDGE ( 'NONE', *, *, #17600, .F. ) ;
#6278=ORIENTED_EDGE ( 'NONE', *, *, #7598, .F. ) ;
#6287=CYLINDRICAL_SURFACE ( 'NONE', #13233, 0.2500000000000002220 ) ;
#6322=CARTESIAN_POINT ( 'NONE',  ( -8.878689293818318209E-17, 6.750000000000000000, 5.100000000000000533 ) ) ;
#6376=CARTESIAN_POINT ( 'NONE',  ( -6.735557395310420329E-17, 6.700000000000000178, 6.299999999999999822 ) ) ;
#6444=AXIS2_PLACEMENT_3D ( 'NONE', #12131, #16105, #11851 ) ;
#6583=EDGE_LOOP ( 'NONE', ( #9958, #11679 ) ) ;
#6590=ORIENTED_EDGE ( 'NONE', *, *, #6705, .F. ) ;
#6664=FACE_OUTER_BOUND ( 'NONE', #3698, .T. ) ;
#6678=PRODUCT ( 'Latch Lock Pin Wire', 'Latch Lock Pin Wire', '', ( #2047 ) ) ;
#6705=EDGE_CURVE ( 'NONE', #12167, #12988, #14691, .T. ) ;
#6727=ORIENTED_EDGE ( 'NONE', *, *, #510, .T. ) ;
#6737=DIRECTION ( 'NONE',  ( -4.177994306516039113E-17, 0.7310552682428709259, -0.6823182503600090376 ) ) ;
#6757=VECTOR ( 'NONE', #11034, 1000.000000000000000 ) ;
#6826=VERTEX_POINT ( 'NONE', #8040 ) ;
#6840=CARTESIAN_POINT ( 'NONE',  ( -6.123233995736763571E-17, 5.318248954186070243, 6.899999999999999467 ) ) ;
#6850=DIRECTION ( 'NONE',  ( 1.059965646700398694E-16, 0.6823182503600109250, 0.7310552682428693716 ) ) ;
#6985=PRODUCT_DEFINITION_SHAPE ( 'NONE', 'NONE',  #4382 ) ;
#6996=ORIENTED_EDGE ( 'NONE', *, *, #15711, .T. ) ;
#7004=EDGE_CURVE ( 'NONE', #6826, #1785, #16990, .T. ) ;
#7047=DIRECTION ( 'NONE',  ( -1.000000000000000000, 0.000000000000000000, 6.123233995736769734E-17 ) ) ;
#7147=EDGE_CURVE ( 'NONE', #12988, #12167, #5533, .T. ) ;
#7169=CYLINDRICAL_SURFACE ( 'NONE', #8567, 0.2499999999999996669 ) ;
#7180=AXIS2_PLACEMENT_3D ( 'NONE', #14872, #3652, #3999 ) ;
#7195=CARTESIAN_POINT ( 'NONE',  ( -1.408343819019460219E-16, 2.299999999999999822, 5.100000000000000533 ) ) ;
#7254=CIRCLE ( 'NONE', #3693, 0.2500000000000002776 ) ;
#7289=FACE_OUTER_BOUND ( 'NONE', #16908, .T. ) ;
#7328=DIRECTION ( 'NONE',  ( -1.224646799147350002E-16, 8.383884571949770538E-16, -1.000000000000000000 ) ) ;
#7363=ORIENTED_EDGE ( 'NONE', *, *, #9175, .T. ) ;
#7382=DIRECTION ( 'NONE',  ( -1.000000000000000000, 0.000000000000000000, 6.123233995736769734E-17 ) ) ;
#7461=ORIENTED_EDGE ( 'NONE', *, *, #13034, .T. ) ;
#7491=DIRECTION ( 'NONE',  ( -1.000000000000000000, 0.000000000000000000, 6.123233995736769734E-17 ) ) ;
#7513=AXIS2_PLACEMENT_3D ( 'NONE', #1666, #8432, #14442 ) ;
#7529=ORIENTED_EDGE ( 'NONE', *, *, #8010, .F. ) ;
#7574=CARTESIAN_POINT ( 'NONE',  ( 1.836970198721020197E-17, 3.581751045813930112, 7.700000000000000178 ) ) ;
#7588=EDGE_CURVE ( 'NONE', #14363, #18075, #513, .T. ) ;
#7598=EDGE_CURVE ( 'NONE', #1106, #1943, #8792, .T. ) ;
#7623=ORIENTED_EDGE ( 'NONE', *, *, #13902, .F. ) ;
#7737=CARTESIAN_POINT ( 'NONE',  ( -6.735557395310440051E-17, 7.000000000000000000, 6.299999999999999822 ) ) ;
#7767=CARTESIAN_POINT ( 'NONE',  ( 1.972152263052529951E-31, 9.299999999999998934, 5.100000000000000533 ) ) ;
#7768=DIRECTION ( 'NONE',  ( -1.000000000000000000, 0.000000000000000000, 6.123233995736769734E-17 ) ) ;
#7791=VERTEX_POINT ( 'NONE', #11858 ) ;
#7793=EDGE_CURVE ( 'NONE', #1785, #10043, #10004, .T. ) ;
#7823=ORIENTED_EDGE ( 'NONE', *, *, #510, .F. ) ;
#7830=DIRECTION ( 'NONE',  ( -6.123233995736769734E-17, 3.749399456654650178E-33, -1.000000000000000000 ) ) ;
#7870=CARTESIAN_POINT ( 'NONE',  ( -6.735557395310420329E-17, 6.700000000000000178, 6.299999999999999822 ) ) ;
#7873=DIRECTION ( 'NONE',  ( 6.123233995736767268E-17, -1.000000000000000000, 0.000000000000000000 ) ) ;
#7927=AXIS2_PLACEMENT_3D ( 'NONE', #3142, #17476, #4796 ) ;
#7959=CARTESIAN_POINT ( 'NONE',  ( 6.735557395310435121E-17, 3.581751045813930112, 8.250000000000000000 ) ) ;
#7985=MANIFOLD_SOLID_BREP ( 'Stock-MAS-687-1', #1085 ) ;
#8010=EDGE_CURVE ( 'NONE', #17654, #1785, #17363, .T. ) ;
#8033=DIRECTION ( 'NONE',  ( 4.476422471267168520E-17, 0.6823182503600082605, 0.7310552682428719251 ) ) ;
#8040=CARTESIAN_POINT ( 'NONE',  ( 3.591599821218599745E-17, 3.615866958331932057, 7.736552763412146483 ) ) ;
#8131=DIRECTION ( 'NONE',  ( 1.000000000000000000, 1.283953296258166085E-32, -6.123233995736769734E-17 ) ) ;
#8160=VECTOR ( 'NONE', #11401, 1000.000000000000000 ) ;
#8188=AXIS2_PLACEMENT_3D ( 'NONE', #11832, #5994, #17454 ) ;
#8271=CARTESIAN_POINT ( 'NONE',  ( -1.255262969126040791E-16, 2.049999999999999822, 5.100000000000000533 ) ) ;
#8278=AXIS2_PLACEMENT_3D ( 'NONE', #209, #15589, #11233 ) ;
#8293=LINE ( 'NONE', #13932, #11712 ) ;
#8300=CARTESIAN_POINT ( 'NONE',  ( -4.898587196589392737E-17, 6.700000000000000178, 6.349999999999999645 ) ) ;
#8368=DIRECTION ( 'NONE',  ( -4.177994306516050823E-17, 0.7310552682428690385, -0.6823182503600111470 ) ) ;
#8432=DIRECTION ( 'NONE',  ( 3.018987445473099952E-48, 1.000000000000000000, 2.465190328815659976E-32 ) ) ;
#8567=AXIS2_PLACEMENT_3D ( 'NONE', #3848, #8368, #12807 ) ;
#8573=DIRECTION ( 'NONE',  ( 6.123233995736823968E-17, 0.000000000000000000, 1.000000000000000000 ) ) ;
#8589=AXIS2_PLACEMENT_3D ( 'NONE', #10895, #7830, #1076 ) ;
#8622=EDGE_CURVE ( 'NONE', #10043, #1106, #16195, .T. ) ;
#8661=DIRECTION ( 'NONE',  ( -4.177994306516050823E-17, 0.7310552682428690385, -0.6823182503600111470 ) ) ;
#8662=EDGE_CURVE ( 'NONE', #15551, #2515, #13259, .T. ) ;
#8700=ORIENTED_EDGE ( 'NONE', *, *, #10764, .T. ) ;
#8755=AXIS2_PLACEMENT_3D ( 'NONE', #9626, #12321, #17847 ) ;
#8757=TOROIDAL_SURFACE ( 'NONE', #16784, 0.2999999999999999889, 0.2500000000000000000 ) ;
#8781=FACE_OUTER_BOUND ( 'NONE', #3356, .T. ) ;
#8792=CIRCLE ( 'NONE', #9077, 0.2500000000000002220 ) ;
#8807=( GEOMETRIC_REPRESENTATION_CONTEXT ( 3 ) GLOBAL_UNCERTAINTY_ASSIGNED_CONTEXT ( ( #13636 ) ) GLOBAL_UNIT_ASSIGNED_CONTEXT ( ( #2591, #12774, #9994 ) ) REPRESENTATION_CONTEXT ( 'NONE', 'WORKASPACE' ) );
#8809=TOROIDAL_SURFACE ( 'NONE', #2608, 0.2999999999999999889, 0.2500000000000000000 ) ;
#8813=ORIENTED_EDGE ( 'NONE', *, *, #7004, .F. ) ;
#8886=DIRECTION ( 'NONE',  ( 6.123233995736768501E-17, 0.000000000000000000, 1.000000000000000000 ) ) ;
#8915=CYLINDRICAL_SURFACE ( 'NONE', #17073, 0.2500000000000002220 ) ;
#9009=VECTOR ( 'NONE', #6240, 1000.000000000000000 ) ;
#9050=VECTOR ( 'NONE', #12588, 1000.000000000000000 ) ;
#9077=AXIS2_PLACEMENT_3D ( 'NONE', #11313, #16865, #18222 ) ;
#9145=FACE_OUTER_BOUND ( 'NONE', #6583, .T. ) ;
#9161=DIRECTION ( 'NONE',  ( -1.000000000000000000, 0.000000000000000000, 6.123233995736769734E-17 ) ) ;
#9175=EDGE_CURVE ( 'NONE', #5801, #2436, #3219, .T. ) ;
#9258=FACE_OUTER_BOUND ( 'NONE', #10378, .T. ) ;
#9473=ORIENTED_EDGE ( 'NONE', *, *, #14466, .F. ) ;
#9550=EDGE_LOOP ( 'NONE', ( #2117, #12812, #4167, #17410 ) ) ;
#9626=CARTESIAN_POINT ( 'NONE',  ( 3.673940397442050254E-17, 2.600000000000000089, 8.000000000000000000 ) ) ;
#9635=CARTESIAN_POINT ( 'NONE',  ( -1.255262969126040791E-16, 2.049999999999999822, 5.100000000000000533 ) ) ;
#9640=CARTESIAN_POINT ( 'NONE',  ( -6.735557395310430190E-17, 7.000000000000000000, 6.299999999999999822 ) ) ;
#9645=AXIS2_PLACEMENT_3D ( 'NONE', #7870, #17760, #16391 ) ;
#9669=AXIS2_PLACEMENT_3D ( 'NONE', #3670, #8131, #2202 ) ;
#9709=( NAMED_UNIT ( * ) SI_UNIT ( $, .STERADIAN. ) SOLID_ANGLE_UNIT ( ) );
#9727=CARTESIAN_POINT ( 'NONE',  ( -1.836970198721025435E-17, 5.318248954186070243, 6.850000000000000533 ) ) ;
#9768=ADVANCED_FACE ( 'NONE', ( #14517 ), #13569, .T. ) ;
#9805=SHAPE_REPRESENTATION_RELATIONSHIP ( 'NONE' , 'NONE' ,  #16473, #4658 ) ;
#9891=ORIENTED_EDGE ( 'NONE', *, *, #10067, .F. ) ;
#9899=CARTESIAN_POINT ( 'NONE',  ( -4.404543739248539922E-17, 5.113553479078069230, 6.680683419527140288 ) ) ;
#9928=CARTESIAN_POINT ( 'NONE',  ( -5.204748896376247618E-17, 7.250000000000000000, 6.299999999999999822 ) ) ;
#9931=FACE_OUTER_BOUND ( 'NONE', #832, .T. ) ;
#9936=ORIENTED_EDGE ( 'NONE', *, *, #1840, .T. ) ;
#9940=TOROIDAL_SURFACE ( 'NONE', #3411, 0.2999999999999999889, 0.2500000000000000000 ) ;
#9958=ORIENTED_EDGE ( 'NONE', *, *, #17600, .T. ) ;
#9993=AXIS2_PLACEMENT_3D ( 'NONE', #1658, #281, #10166 ) ;
#9994=( NAMED_UNIT ( * ) SI_UNIT ( $, .STERADIAN. ) SOLID_ANGLE_UNIT ( ) );
#10004=CIRCLE ( 'NONE', #7927, 0.5500000000000001554 ) ;
#10043=VERTEX_POINT ( 'NONE', #15238 ) ;
#10067=EDGE_CURVE ( 'NONE', #7791, #5801, #16241, .T. ) ;
#10094=ADVANCED_FACE ( 'NONE', ( #9931 ), #7169, .T. ) ;
#10106=DIRECTION ( 'NONE',  ( 3.018987445473099952E-48, 1.000000000000000000, 2.465190328815659976E-32 ) ) ;
#10166=DIRECTION ( 'NONE',  ( 1.224646799147349016E-16, 0.000000000000000000, 1.000000000000000000 ) ) ;
#10246=EDGE_CURVE ( 'NONE', #2515, #15551, #13589, .T. ) ;
#10284=LINE ( 'NONE', #9928, #14706 ) ;
#10327=CARTESIAN_POINT ( 'NONE',  ( -4.404543739248539922E-17, 5.113553479078069230, 6.680683419527140288 ) ) ;
#10343=DIRECTION ( 'NONE',  ( -6.161988852941170860E-64, -1.000000000000000000, 3.773129962568039733E-80 ) ) ;
#10347=AXIS2_PLACEMENT_3D ( 'NONE', #17806, #3653, #8033 ) ;
#10378=EDGE_LOOP ( 'NONE', ( #799, #6996, #18157, #16351 ) ) ;
#10453=CARTESIAN_POINT ( 'NONE',  ( -4.592425496802605650E-17, 2.550000000000000266, 7.700000000000000178 ) ) ;
#10607=CYLINDRICAL_SURFACE ( 'NONE', #8589, 0.2500000000000002220 ) ;
#10625=CARTESIAN_POINT ( 'NONE',  ( 3.673940397442059498E-17, 2.600000000000000089, 8.000000000000000000 ) ) ;
#10630=ORIENTED_EDGE ( 'NONE', *, *, #8622, .T. ) ;
#10638=ORIENTED_EDGE ( 'NONE', *, *, #11485, .F. ) ;
#10715=DIRECTION ( 'NONE',  ( 6.123233995736806712E-17, 0.000000000000000000, 1.000000000000000000 ) ) ;
#10764=EDGE_CURVE ( 'NONE', #2515, #5242, #895, .T. ) ;
#10780=EDGE_CURVE ( 'NONE', #18075, #14363, #5915, .T. ) ;
#10824=AXIS2_PLACEMENT_3D ( 'NONE', #6017, #2734, #8886 ) ;
#10847=UNCERTAINTY_MEASURE_WITH_UNIT (LENGTH_MEASURE( 1.000000000000000082E-05 ), #5546, 'distance_accuracy_value', 'NONE');
#10895=CARTESIAN_POINT ( 'NONE',  ( -6.735557395310440051E-17, 7.000000000000000000, 6.299999999999999822 ) ) ;
#10981=ORIENTED_EDGE ( 'NONE', *, *, #15378, .F. ) ;
#11034=DIRECTION ( 'NONE',  ( 6.123233995736769734E-17, 8.894960955186829541E-48, 1.000000000000000000 ) ) ;
#11060=ORIENTED_EDGE ( 'NONE', *, *, #13034, .F. ) ;
#11097=EDGE_LOOP ( 'NONE', ( #5325, #9936, #13077, #6278 ) ) ;
#11191=CARTESIAN_POINT ( 'NONE',  ( 0.000000000000000000, 0.000000000000000000, 0.000000000000000000 ) ) ;
#11197=CIRCLE ( 'NONE', #14446, 0.2500000000000002220 ) ;
#11233=DIRECTION ( 'NONE',  ( 6.123233995736764803E-17, -1.000000000000000000, 0.000000000000000000 ) ) ;
#11288=EDGE_CURVE ( 'NONE', #17654, #4420, #11838, .T. ) ;
#11313=CARTESIAN_POINT ( 'NONE',  ( -4.898587196589400133E-17, 6.700000000000000178, 6.599999999999999645 ) ) ;
#11369=DIRECTION ( 'NONE',  ( -6.123233995736794386E-17, 0.000000000000000000, -1.000000000000000000 ) ) ;
#11384=CARTESIAN_POINT ( 'NONE',  ( 1.836970198721020197E-17, 3.581751045813930112, 7.700000000000000178 ) ) ;
#11401=DIRECTION ( 'NONE',  ( -6.123233995736769734E-17, 3.749399456654650178E-33, -1.000000000000000000 ) ) ;
#11445=AXIS2_PLACEMENT_3D ( 'NONE', #5841, #2987, #5479 ) ;
#11448=CARTESIAN_POINT ( 'NONE',  ( -3.061616997868380553E-17, 5.318248954186070243, 6.899999999999999467 ) ) ;
#11485=EDGE_CURVE ( 'NONE', #5242, #6826, #17144, .T. ) ;
#11491=VECTOR ( 'NONE', #13905, 1000.000000000000000 ) ;
#11551=ADVANCED_FACE ( 'NONE', ( #5143 ), #10607, .T. ) ;
#11564=ORIENTED_EDGE ( 'NONE', *, *, #7147, .F. ) ;
#11642=CARTESIAN_POINT ( 'NONE',  ( -8.878689293818279999E-17, 6.750000000000000000, 6.300000000000002487 ) ) ;
#11676=EDGE_CURVE ( 'NONE', #16660, #2436, #13915, .T. ) ;
#11679=ORIENTED_EDGE ( 'NONE', *, *, #4349, .T. ) ;
#11689=ORIENTED_EDGE ( 'NONE', *, *, #16019, .F. ) ;
#11691=DIRECTION ( 'NONE',  ( 0.000000000000000000, 1.000000000000000000, 0.000000000000000000 ) ) ;
#11712=VECTOR ( 'NONE', #1249, 1000.000000000000000 ) ;
#11728=ORIENTED_EDGE ( 'NONE', *, *, #417, .F. ) ;
#11731=CARTESIAN_POINT ( 'NONE',  ( 1.836970198721020197E-17, 2.600000000000000089, 7.700000000000000178 ) ) ;
#11832=CARTESIAN_POINT ( 'NONE',  ( -1.408343819019460219E-16, 2.299999999999999822, 5.100000000000000533 ) ) ;
#11838=CIRCLE ( 'NONE', #1499, 0.04999999999999969746 ) ;
#11851=DIRECTION ( 'NONE',  ( 1.224646799147349263E-16, 0.000000000000000000, 1.000000000000000000 ) ) ;
#11858=CARTESIAN_POINT ( 'NONE',  ( 3.367778697655222491E-17, 2.049999999999999822, 7.700000000000000178 ) ) ;
#11923=FACE_OUTER_BOUND ( 'NONE', #12665, .T. ) ;
#11941=CARTESIAN_POINT ( 'NONE',  ( 3.673940397442067510E-17, 2.600000000000000089, 7.750000000000000000 ) ) ;
#12024=ORIENTED_EDGE ( 'NONE', *, *, #207, .T. ) ;
#12088=AXIS2_PLACEMENT_3D ( 'NONE', #1681, #5936, #814 ) ;
#12131=CARTESIAN_POINT ( 'NONE',  ( 3.673940397442059498E-17, 3.581751045813930112, 8.000000000000000000 ) ) ;
#12167=VERTEX_POINT ( 'NONE', #13031 ) ;
#12246=FACE_OUTER_BOUND ( 'NONE', #16059, .T. ) ;
#12321=DIRECTION ( 'NONE',  ( 3.749399456654639914E-33, 1.000000000000000000, 6.123233995736769734E-17 ) ) ;
#12377=CIRCLE ( 'NONE', #15040, 0.2500000000000002220 ) ;
#12468=CARTESIAN_POINT ( 'NONE',  ( -1.754629622497533634E-17, 5.284133041668071407, 6.863447236587855826 ) ) ;
#12495=PRESENTATION_STYLE_ASSIGNMENT (( #4 ) ) ;
#12557=CARTESIAN_POINT ( 'NONE',  ( -1.408343819019460219E-16, 7.000000000000000000, 5.100000000000000533 ) ) ;
#12588=DIRECTION ( 'NONE',  ( 0.000000000000000000, 1.000000000000000000, 0.000000000000000000 ) ) ;
#12630=CARTESIAN_POINT ( 'NONE',  ( 5.829811056852225605E-17, 3.957026083511936854, 8.102080397533582001 ) ) ;
#12635=AXIS2_PLACEMENT_3D ( 'NONE', #1089, #6737, #13691 ) ;
#12639=DIRECTION ( 'NONE',  ( 6.123233995736769734E-17, -1.368455531567203867E-48, 1.000000000000000000 ) ) ;
#12665=EDGE_LOOP ( 'NONE', ( #18138, #6727, #13009, #17754 ) ) ;
#12670=CYLINDRICAL_SURFACE ( 'NONE', #5717, 0.2499999999999996669 ) ;
#12699=( GEOMETRIC_REPRESENTATION_CONTEXT ( 3 ) GLOBAL_UNCERTAINTY_ASSIGNED_CONTEXT ( ( #10847 ) ) GLOBAL_UNIT_ASSIGNED_CONTEXT ( ( #5546, #14154, #9709 ) ) REPRESENTATION_CONTEXT ( 'NONE', 'WORKASPACE' ) );
#12710=LINE ( 'NONE', #8271, #6757 ) ;
#12724=ORIENTED_EDGE ( 'NONE', *, *, #13902, .T. ) ;
#12774=( NAMED_UNIT ( * ) PLANE_ANGLE_UNIT ( ) SI_UNIT ( $, .RADIAN. ) );
#12807=DIRECTION ( 'NONE',  ( 1.059965646700401283E-16, 0.6823182503600125903, 0.7310552682428677063 ) ) ;
#12812=ORIENTED_EDGE ( 'NONE', *, *, #4805, .T. ) ;
#12921=VECTOR ( 'NONE', #8661, 1000.000000000000000 ) ;
#12935=CYLINDRICAL_SURFACE ( 'NONE', #2774, 0.2500000000000002220 ) ;
#12983=CARTESIAN_POINT ( 'NONE',  ( 3.673940397442059498E-17, 3.581751045813930112, 8.000000000000000000 ) ) ;
#12988=VERTEX_POINT ( 'NONE', #9635 ) ;
#13009=ORIENTED_EDGE ( 'NONE', *, *, #15378, .T. ) ;
#13031=CARTESIAN_POINT ( 'NONE',  ( -4.592425496802619825E-17, 2.550000000000000266, 5.100000000000000533 ) ) ;
#13034=EDGE_CURVE ( 'NONE', #12167, #5801, #15402, .T. ) ;
#13062=DIRECTION ( 'NONE',  ( 6.123233995736767268E-17, 1.000000000000000000, 0.000000000000000000 ) ) ;
#13077=ORIENTED_EDGE ( 'NONE', *, *, #6108, .T. ) ;
#13139=DIRECTION ( 'NONE',  ( -6.740754805355319355E-31, 1.000000000000000000, -1.040834085586083310E-14 ) ) ;
#13142=ORIENTED_EDGE ( 'NONE', *, *, #4805, .F. ) ;
#13208=CIRCLE ( 'NONE', #12635, 0.2500000000000006106 ) ;
#13233=AXIS2_PLACEMENT_3D ( 'NONE', #2036, #3334, #7873 ) ;
#13254=CYLINDRICAL_SURFACE ( 'NONE', #2336, 0.2500000000000002220 ) ;
#13259=CIRCLE ( 'NONE', #6444, 0.2500000000000002220 ) ;
#13321=CARTESIAN_POINT ( 'NONE',  ( -4.898587196589392737E-17, 5.318248954186070243, 6.349999999999999645 ) ) ;
#13323=ORIENTED_EDGE ( 'NONE', *, *, #5645, .T. ) ;
#13345=CARTESIAN_POINT ( 'NONE',  ( -1.408343819019460219E-16, 2.299999999999999822, 5.100000000000000533 ) ) ;
#13398=CYLINDRICAL_SURFACE ( 'NONE', #17940, 0.2500000000000002220 ) ;
#13412=DIRECTION ( 'NONE',  ( -1.224646799147350002E-16, 8.383884571949770538E-16, -1.000000000000000000 ) ) ;
#13465=DIRECTION ( 'NONE',  ( 5.296209390990920866E-31, 1.000000000000000000, 8.548717289613711672E-15 ) ) ;
#13540=STYLED_ITEM ( 'NONE', ( #12495 ), #7985 ) ;
#13569=TOROIDAL_SURFACE ( 'NONE', #4998, 0.2999999999999999889, 0.2500000000000000000 ) ;
#13589=CIRCLE ( 'NONE', #2355, 0.2500000000000002220 ) ;
#13597=CARTESIAN_POINT ( 'NONE',  ( -3.673940397442036695E-17, 6.700000000000000178, 6.299999999999999822 ) ) ;
#13636=UNCERTAINTY_MEASURE_WITH_UNIT (LENGTH_MEASURE( 1.000000000000000082E-05 ), #2591, 'distance_accuracy_value', 'NONE');
#13691=DIRECTION ( 'NONE',  ( 4.476422471267168520E-17, 0.6823182503600082605, 0.7310552682428719251 ) ) ;
#13787=SURFACE_SIDE_STYLE ('',( #13969 ) ) ;
#13862=VECTOR ( 'NONE', #14704, 1000.000000000000000 ) ;
#13902=EDGE_CURVE ( 'NONE', #15551, #6826, #15307, .T. ) ;
#13905=DIRECTION ( 'NONE',  ( 6.123233995736769734E-17, 8.894960955186829541E-48, 1.000000000000000000 ) ) ;
#13915=CIRCLE ( 'NONE', #2385, 0.2500000000000002220 ) ;
#13932=CARTESIAN_POINT ( 'NONE',  ( 6.735557395310435121E-17, 2.600000000000000089, 8.250000000000000000 ) ) ;
#13948=DIRECTION ( 'NONE',  ( -1.224646799147350002E-16, 8.383884571949770538E-16, -1.000000000000000000 ) ) ;
#13969=SURFACE_STYLE_FILL_AREA ( #2863 ) ;
#14042=EDGE_CURVE ( 'NONE', #2436, #15551, #17477, .T. ) ;
#14120=CARTESIAN_POINT ( 'NONE',  ( 3.673940397442050254E-17, 2.600000000000000089, 8.000000000000000000 ) ) ;
#14154=( NAMED_UNIT ( * ) PLANE_ANGLE_UNIT ( ) SI_UNIT ( $, .RADIAN. ) );
#14223=DIRECTION ( 'NONE',  ( 3.749399456654639914E-33, 1.000000000000000000, 6.123233995736769734E-17 ) ) ;
#14230=CARTESIAN_POINT ( 'NONE',  ( 1.836970198721020197E-17, 2.600000000000000089, 7.700000000000000178 ) ) ;
#14274=LINE ( 'NONE', #15579, #8160 ) ;
#14363=VERTEX_POINT ( 'NONE', #11642 ) ;
#14394=ADVANCED_FACE ( 'NONE', ( #11923 ), #13398, .T. ) ;
#14442=DIRECTION ( 'NONE',  ( 1.224646799147349263E-16, 0.000000000000000000, 1.000000000000000000 ) ) ;
#14446=AXIS2_PLACEMENT_3D ( 'NONE', #12557, #13948, #2556 ) ;
#14466=EDGE_CURVE ( 'NONE', #1106, #14363, #15027, .T. ) ;
#14517=FACE_OUTER_BOUND ( 'NONE', #1359, .T. ) ;
#14632=EDGE_LOOP ( 'NONE', ( #1078, #15180, #12724, #10638 ) ) ;
#14691=CIRCLE ( 'NONE', #8188, 0.2500000000000002220 ) ;
#14704=DIRECTION ( 'NONE',  ( 0.000000000000000000, 1.000000000000000000, 0.000000000000000000 ) ) ;
#14706=VECTOR ( 'NONE', #4269, 1000.000000000000000 ) ;
#14729=CARTESIAN_POINT ( 'NONE',  ( -6.735557395310447447E-17, 7.250000000000000000, 6.299999999999997158 ) ) ;
#14770=AXIS2_PLACEMENT_3D ( 'NONE', #284, #5923, #13139 ) ;
#14806=PLANE ( 'NONE',  #3674 ) ;
#14872=CARTESIAN_POINT ( 'NONE',  ( -4.898587196589400133E-17, 5.318248954186070243, 6.599999999999999645 ) ) ;
#14887=DIRECTION ( 'NONE',  ( 3.018987445473099952E-48, 1.000000000000000000, 2.465190328815659976E-32 ) ) ;
#14889=FACE_OUTER_BOUND ( 'NONE', #4143, .T. ) ;
#14927=ADVANCED_FACE ( 'NONE', ( #341 ), #8757, .T. ) ;
#15025=TOROIDAL_SURFACE ( 'NONE', #4062, 0.2999999999999999889, 0.2500000000000000000 ) ;
#15027=CIRCLE ( 'NONE', #15865, 0.04999999999999969746 ) ;
#15040=AXIS2_PLACEMENT_3D ( 'NONE', #3145, #7328, #13062 ) ;
#15180=ORIENTED_EDGE ( 'NONE', *, *, #10246, .T. ) ;
#15238=CARTESIAN_POINT ( 'NONE',  ( -4.898587196589392737E-17, 5.318248954186071131, 6.349999999999999645 ) ) ;
#15305=TOROIDAL_SURFACE ( 'NONE', #9669, 0.2999999999999999889, 0.2500000000000000000 ) ;
#15307=CIRCLE ( 'NONE', #11445, 0.04999999999999969746 ) ;
#15320=AXIS2_PLACEMENT_3D ( 'NONE', #343, #7382, #15892 ) ;
#15355=VERTEX_POINT ( 'NONE', #2643 ) ;
#15378=EDGE_CURVE ( 'NONE', #16660, #2515, #8293, .T. ) ;
#15388=DIRECTION ( 'NONE',  ( 0.000000000000000000, 1.000000000000000000, 0.000000000000000000 ) ) ;
#15402=LINE ( 'NONE', #3986, #11491 ) ;
#15422=ORIENTED_EDGE ( 'NONE', *, *, #14042, .T. ) ;
#15446=CARTESIAN_POINT ( 'NONE',  ( 3.591599821218572011E-17, 3.615866958331936942, 7.736552763412142042 ) ) ;
#15526=CARTESIAN_POINT ( 'NONE',  ( 1.836970198721030057E-17, 2.299999999999999822, 7.700000000000000178 ) ) ;
#15551=VERTEX_POINT ( 'NONE', #1115 ) ;
#15579=CARTESIAN_POINT ( 'NONE',  ( -5.204748896376249466E-17, 6.750000000000000000, 6.299999999999999822 ) ) ;
#15589=DIRECTION ( 'NONE',  ( 6.123233995736769734E-17, -1.368455531567203867E-48, 1.000000000000000000 ) ) ;
#15600=TOROIDAL_SURFACE ( 'NONE', #15878, 0.2999999999999999889, 0.2500000000000000000 ) ;
#15650=ORIENTED_EDGE ( 'NONE', *, *, #417, .T. ) ;
#15711=EDGE_CURVE ( 'NONE', #1943, #1106, #6106, .T. ) ;
#15728=DIRECTION ( 'NONE',  ( 1.059965646700401283E-16, 0.6823182503600125903, 0.7310552682428677063 ) ) ;
#15833=DIRECTION ( 'NONE',  ( 6.123233995736768501E-17, 0.000000000000000000, 1.000000000000000000 ) ) ;
#15865=AXIS2_PLACEMENT_3D ( 'NONE', #13597, #16272, #10715 ) ;
#15878=AXIS2_PLACEMENT_3D ( 'NONE', #1929, #7768, #6097 ) ;
#15883=AXIS2_PLACEMENT_3D ( 'NONE', #7195, #1633, #5624 ) ;
#15892=DIRECTION ( 'NONE',  ( 6.123233995736767268E-17, 0.000000000000000000, 1.000000000000000000 ) ) ;
#15917=CIRCLE ( 'NONE', #6138, 0.2500000000000002220 ) ;
#15955=ADVANCED_FACE ( 'NONE', ( #14889 ), #15305, .T. ) ;
#15961=DIRECTION ( 'NONE',  ( 6.123233995736767268E-17, -1.000000000000000000, 0.000000000000000000 ) ) ;
#16019=EDGE_CURVE ( 'NONE', #6826, #5242, #13208, .T. ) ;
#16059=EDGE_LOOP ( 'NONE', ( #11564, #6590 ) ) ;
#16105=DIRECTION ( 'NONE',  ( 3.018987445473109675E-48, 1.000000000000000000, 2.465190328815659976E-32 ) ) ;
#16195=LINE ( 'NONE', #13321, #13862 ) ;
#16205=MECHANICAL_DESIGN_GEOMETRIC_PRESENTATION_REPRESENTATION('',(#13540),#8807);
#16215=ORIENTED_EDGE ( 'NONE', *, *, #15711, .F. ) ;
#16241=CIRCLE ( 'NONE', #8278, 0.2500000000000002220 ) ;
#16272=DIRECTION ( 'NONE',  ( -1.000000000000000000, 0.000000000000000000, 6.123233995736769734E-17 ) ) ;
#16349=EDGE_CURVE ( 'NONE', #1943, #18075, #4936, .T. ) ;
#16351=ORIENTED_EDGE ( 'NONE', *, *, #10780, .F. ) ;
#16378=ORIENTED_EDGE ( 'NONE', *, *, #10067, .T. ) ;
#16391=DIRECTION ( 'NONE',  ( 6.123233995736769734E-17, 9.462128050782581713E-15, 1.000000000000000000 ) ) ;
#16432=ORIENTED_EDGE ( 'NONE', *, *, #207, .F. ) ;
#16442=ORIENTED_EDGE ( 'NONE', *, *, #17371, .F. ) ;
#16454=ADVANCED_FACE ( 'NONE', ( #3293 ), #15025, .T. ) ;
#16473=SHAPE_REPRESENTATION ( 'Latch Lock Pin Wire', ( #17681 ), #12699 ) ;
#16506=CARTESIAN_POINT ( 'NONE',  ( 0.000000000000000000, 0.000000000000000000, 5.100000000000000533 ) ) ;
#16510=EDGE_CURVE ( 'NONE', #4420, #10043, #3757, .T. ) ;
#16640=ORIENTED_EDGE ( 'NONE', *, *, #11485, .T. ) ;
#16660=VERTEX_POINT ( 'NONE', #4115 ) ;
#16741=CIRCLE ( 'NONE', #8755, 0.2500000000000002220 ) ;
#16774=AXIS2_PLACEMENT_3D ( 'NONE', #16506, #5206, #3820 ) ;
#16784=AXIS2_PLACEMENT_3D ( 'NONE', #14230, #3200, #1550 ) ;
#16836=DIRECTION ( 'NONE',  ( 0.000000000000000000, 0.000000000000000000, 1.000000000000000000 ) ) ;
#16861=ORIENTED_EDGE ( 'NONE', *, *, #7598, .T. ) ;
#16865=DIRECTION ( 'NONE',  ( 0.000000000000000000, 1.000000000000000000, 0.000000000000000000 ) ) ;
#16908=EDGE_LOOP ( 'NONE', ( #5785, #12024, #6273, #5690 ) ) ;
#16913=APPLICATION_CONTEXT ( 'automotive_design' ) ;
#16941=FACE_OUTER_BOUND ( 'NONE', #17950, .T. ) ;
#16990=LINE ( 'NONE', #15446, #12921 ) ;
#17001=DIRECTION ( 'NONE',  ( -4.177994306516050823E-17, 0.7310552682428690385, -0.6823182503600111470 ) ) ;
#17073=AXIS2_PLACEMENT_3D ( 'NONE', #3275, #11691, #2157 ) ;
#17090=CARTESIAN_POINT ( 'NONE',  ( 3.179896940101190659E-17, 3.786446520921940007, 7.919316580472860245 ) ) ;
#17144=CIRCLE ( 'NONE', #10347, 0.2500000000000006106 ) ;
#17214=ORIENTED_EDGE ( 'NONE', *, *, #6108, .F. ) ;
#17363=CIRCLE ( 'NONE', #529, 0.2500000000000002776 ) ;
#17365=DIRECTION ( 'NONE',  ( -1.000000000000000000, 6.161988852941170860E-64, 6.123233995736769734E-17 ) ) ;
#17371=EDGE_CURVE ( 'NONE', #5801, #7791, #15917, .T. ) ;
#17383=ORIENTED_EDGE ( 'NONE', *, *, #16019, .T. ) ;
#17410=ORIENTED_EDGE ( 'NONE', *, *, #1840, .F. ) ;
#17419=AXIS2_PLACEMENT_3D ( 'NONE', #7574, #7491, #15833 ) ;
#17454=DIRECTION ( 'NONE',  ( 6.123233995736767268E-17, -1.000000000000000000, 0.000000000000000000 ) ) ;
#17476=DIRECTION ( 'NONE',  ( 1.000000000000000000, 1.283953296258166085E-32, -6.123233995736769734E-17 ) ) ;
#17477=LINE ( 'NONE', #11941, #17625 ) ;
#17503=FACE_OUTER_BOUND ( 'NONE', #11097, .T. ) ;
#17508=ORIENTED_EDGE ( 'NONE', *, *, #7588, .F. ) ;
#17600=EDGE_CURVE ( 'NONE', #15355, #4874, #11197, .T. ) ;
#17625=VECTOR ( 'NONE', #10106, 1000.000000000000000 ) ;
#17654=VERTEX_POINT ( 'NONE', #12468 ) ;
#17681=AXIS2_PLACEMENT_3D ( 'NONE', #11191, #16836, #4146 ) ;
#17705=DIRECTION ( 'NONE',  ( 1.059965646700398694E-16, 0.6823182503600109250, 0.7310552682428693716 ) ) ;
#17754=ORIENTED_EDGE ( 'NONE', *, *, #8662, .F. ) ;
#17760=DIRECTION ( 'NONE',  ( -1.000000000000000000, 0.000000000000000000, 6.123233995736769734E-17 ) ) ;
#17771=EDGE_LOOP ( 'NONE', ( #156, #7461, #9891, #6224 ) ) ;
#17806=CARTESIAN_POINT ( 'NONE',  ( 3.179896940101190659E-17, 3.786446520921929793, 7.919316580472860245 ) ) ;
#17819=DIRECTION ( 'NONE',  ( 1.224646799147349263E-16, 0.000000000000000000, 1.000000000000000000 ) ) ;
#17847=DIRECTION ( 'NONE',  ( 6.123233995736823968E-17, 0.000000000000000000, 1.000000000000000000 ) ) ;
#17868=PLANE ( 'NONE',  #16774 ) ;
#17872=ORIENTED_EDGE ( 'NONE', *, *, #8010, .T. ) ;
#17888=CARTESIAN_POINT ( 'NONE',  ( -4.898587196589400133E-17, 5.318248954186070243, 6.599999999999999645 ) ) ;
#17940=AXIS2_PLACEMENT_3D ( 'NONE', #10625, #14887, #17819 ) ;
#17950=EDGE_LOOP ( 'NONE', ( #3370, #15422, #1610, #10981 ) ) ;
#18050=ADVANCED_FACE ( 'NONE', ( #395 ), #13254, .T. ) ;
#18075=VERTEX_POINT ( 'NONE', #14729 ) ;
#18138=ORIENTED_EDGE ( 'NONE', *, *, #14042, .F. ) ;
#18157=ORIENTED_EDGE ( 'NONE', *, *, #14466, .T. ) ;
#18222=DIRECTION ( 'NONE',  ( 1.224646799147349016E-16, 0.000000000000000000, 1.000000000000000000 ) ) ;
#18264=DIRECTION ( 'NONE',  ( 6.123233995736764803E-17, -1.000000000000000000, 0.000000000000000000 ) ) ;
ENDSEC;
END-ISO-10303-21;
